ISO-10303-21;
HEADER;
/* Generated by software containing ST-Developer
 * from STEP Tools, Inc. (www.steptools.com) 
 */
/* OPTION: using custom renumber hook */

FILE_DESCRIPTION(
/* description */ ('STEP AP242 Edition 2', 'CAx-IF Rec.Pracs.---Representation and Presentation of Product Manufa
cturing Information (PMI)---4.0---2014-10-13', 'CAx-IF Rec.Pracs.---3D Tessellated Geometry---0.4---2014-09-14', '2;1', 'CAx-IF Rec.Pracs.---User Defined Attributes---1.5---2016-08-15'),
/* implementation_level */ '2;1');

FILE_NAME(
/* name */ 'ball_retainer.step',
/* time_stamp */ '2026-10-08T12:15:07Z',
/* author */ (''),
/* organization */ (''),
/* preprocessor_version */ 'ST-DEVELOPER v20',
/* originating_system */ 'ONSHAPE BY PTC INC, 1.221',
/* authorisation */ '  ');

FILE_SCHEMA (('AP242_MANAGED_MODEL_BASED_3D_ENGINEERING_MIM_LF { 1 0 10303 442 3 1 4 }'));
ENDSEC;

DATA;
#32=CONICAL_SURFACE('',#15246,0.003,0.49057568292852);
#33=CONICAL_SURFACE('',#15247,0.003,0.49057568292852);
#34=CONICAL_SURFACE('',#15248,0.003,0.49057568292852);
#35=CONICAL_SURFACE('',#15249,0.006,0.490575682928521);
#36=CONICAL_SURFACE('',#15250,0.006,0.490575682928521);
#37=CONICAL_SURFACE('',#15251,0.006,0.490575682928521);
#38=CONICAL_SURFACE('',#15253,0.006,0.490575682928521);
#39=CONICAL_SURFACE('',#15257,0.003,0.49057568292852);
#60=COLOUR_RGB('', 0.66274510, 0.83137255, 0.94901961);
#225=SHAPE_REPRESENTATION_RELATIONSHIP('','',#13799,#252);
#252=ADVANCED_BREP_SHAPE_REPRESENTATION('',(#13743),#45489);
#331=TOROIDAL_SURFACE('',#15256,0.0077,0.0003);
#1009=CIRCLE('',#15192,0.006);
#1010=CIRCLE('',#15193,0.006);
#1011=CIRCLE('',#15196,0.003);
#1012=CIRCLE('',#15197,0.003);
#1013=CIRCLE('',#15200,0.006);
#1014=CIRCLE('',#15201,0.006);
#1015=CIRCLE('',#15204,0.003);
#1016=CIRCLE('',#15205,0.003);
#1017=CIRCLE('',#15208,0.006);
#1018=CIRCLE('',#15209,0.006);
#1019=CIRCLE('',#15212,0.003);
#1020=CIRCLE('',#15213,0.003);
#1021=CIRCLE('',#15216,0.006);
#1022=CIRCLE('',#15217,0.006);
#1023=CIRCLE('',#15220,0.003);
#1024=CIRCLE('',#15221,0.003);
#1025=CIRCLE('',#15223,0.00180420299878392);
#1026=CIRCLE('',#15224,0.003);
#1027=CIRCLE('',#15225,0.003);
#1028=CIRCLE('',#15226,0.003);
#1029=CIRCLE('',#15227,0.003);
#1030=CIRCLE('',#15229,0.0077);
#1031=CIRCLE('',#15230,0.0043976164792475);
#1032=CIRCLE('',#15231,0.0043976164792475);
#1033=CIRCLE('',#15232,0.0043976164792475);
#1034=CIRCLE('',#15233,0.0043976164792475);
#1035=CIRCLE('',#15235,0.008);
#1036=CIRCLE('',#15236,0.006);
#1037=CIRCLE('',#15237,0.006);
#1038=CIRCLE('',#15238,0.006);
#1039=CIRCLE('',#15239,0.006);
#1040=CIRCLE('',#15241,0.003);
#1041=CIRCLE('',#15242,0.003);
#1042=CIRCLE('',#15243,0.003);
#1043=CIRCLE('',#15244,0.003);
#1044=CIRCLE('',#15245,0.00180420299878392);
#1045=CIRCLE('',#15255,0.008);
#1523=PLANE('',#15190);
#1524=PLANE('',#15194);
#1525=PLANE('',#15198);
#1526=PLANE('',#15202);
#1527=PLANE('',#15206);
#1528=PLANE('',#15210);
#1529=PLANE('',#15214);
#1530=PLANE('',#15218);
#1531=PLANE('',#15222);
#1532=PLANE('',#15228);
#1533=PLANE('',#15234);
#1534=PLANE('',#15240);
#1809=CYLINDRICAL_SURFACE('',#15191,0.006);
#1810=CYLINDRICAL_SURFACE('',#15195,0.003);
#1811=CYLINDRICAL_SURFACE('',#15199,0.006);
#1812=CYLINDRICAL_SURFACE('',#15203,0.003);
#1813=CYLINDRICAL_SURFACE('',#15207,0.006);
#1814=CYLINDRICAL_SURFACE('',#15211,0.003);
#1815=CYLINDRICAL_SURFACE('',#15215,0.006);
#1816=CYLINDRICAL_SURFACE('',#15219,0.003);
#1817=CYLINDRICAL_SURFACE('',#15252,0.00180420299878392);
#1818=CYLINDRICAL_SURFACE('',#15254,0.008);
#5340=ORIENTED_EDGE('',*,*,#7317,.T.);
#5341=ORIENTED_EDGE('',*,*,#7318,.F.);
#5342=ORIENTED_EDGE('',*,*,#7319,.T.);
#5343=ORIENTED_EDGE('',*,*,#7320,.T.);
#5344=ORIENTED_EDGE('',*,*,#7321,.T.);
#5345=ORIENTED_EDGE('',*,*,#7322,.T.);
#5346=ORIENTED_EDGE('',*,*,#7323,.F.);
#5347=ORIENTED_EDGE('',*,*,#7324,.T.);
#5348=ORIENTED_EDGE('',*,*,#7318,.T.);
#5349=ORIENTED_EDGE('',*,*,#7325,.T.);
#5350=ORIENTED_EDGE('',*,*,#7326,.F.);
#5351=ORIENTED_EDGE('',*,*,#7327,.T.);
#5352=ORIENTED_EDGE('',*,*,#7328,.T.);
#5353=ORIENTED_EDGE('',*,*,#7323,.T.);
#5354=ORIENTED_EDGE('',*,*,#7329,.F.);
#5355=ORIENTED_EDGE('',*,*,#7326,.T.);
#5356=ORIENTED_EDGE('',*,*,#7330,.T.);
#5357=ORIENTED_EDGE('',*,*,#7321,.F.);
#5358=ORIENTED_EDGE('',*,*,#7331,.T.);
#5359=ORIENTED_EDGE('',*,*,#7332,.F.);
#5360=ORIENTED_EDGE('',*,*,#7333,.T.);
#5361=ORIENTED_EDGE('',*,*,#7334,.T.);
#5362=ORIENTED_EDGE('',*,*,#7335,.T.);
#5363=ORIENTED_EDGE('',*,*,#7336,.T.);
#5364=ORIENTED_EDGE('',*,*,#7337,.F.);
#5365=ORIENTED_EDGE('',*,*,#7338,.T.);
#5366=ORIENTED_EDGE('',*,*,#7332,.T.);
#5367=ORIENTED_EDGE('',*,*,#7339,.T.);
#5368=ORIENTED_EDGE('',*,*,#7340,.F.);
#5369=ORIENTED_EDGE('',*,*,#7341,.T.);
#5370=ORIENTED_EDGE('',*,*,#7342,.T.);
#5371=ORIENTED_EDGE('',*,*,#7337,.T.);
#5372=ORIENTED_EDGE('',*,*,#7343,.F.);
#5373=ORIENTED_EDGE('',*,*,#7340,.T.);
#5374=ORIENTED_EDGE('',*,*,#7344,.T.);
#5375=ORIENTED_EDGE('',*,*,#7335,.F.);
#5376=ORIENTED_EDGE('',*,*,#7345,.T.);
#5377=ORIENTED_EDGE('',*,*,#7346,.F.);
#5378=ORIENTED_EDGE('',*,*,#7347,.T.);
#5379=ORIENTED_EDGE('',*,*,#7348,.T.);
#5380=ORIENTED_EDGE('',*,*,#7349,.T.);
#5381=ORIENTED_EDGE('',*,*,#7350,.T.);
#5382=ORIENTED_EDGE('',*,*,#7351,.F.);
#5383=ORIENTED_EDGE('',*,*,#7352,.T.);
#5384=ORIENTED_EDGE('',*,*,#7346,.T.);
#5385=ORIENTED_EDGE('',*,*,#7353,.T.);
#5386=ORIENTED_EDGE('',*,*,#7354,.F.);
#5387=ORIENTED_EDGE('',*,*,#7355,.T.);
#5388=ORIENTED_EDGE('',*,*,#7356,.T.);
#5389=ORIENTED_EDGE('',*,*,#7351,.T.);
#5390=ORIENTED_EDGE('',*,*,#7357,.F.);
#5391=ORIENTED_EDGE('',*,*,#7354,.T.);
#5392=ORIENTED_EDGE('',*,*,#7358,.T.);
#5393=ORIENTED_EDGE('',*,*,#7349,.F.);
#5394=ORIENTED_EDGE('',*,*,#7359,.T.);
#5395=ORIENTED_EDGE('',*,*,#7360,.F.);
#5396=ORIENTED_EDGE('',*,*,#7361,.T.);
#5397=ORIENTED_EDGE('',*,*,#7362,.T.);
#5398=ORIENTED_EDGE('',*,*,#7363,.T.);
#5399=ORIENTED_EDGE('',*,*,#7364,.F.);
#5400=ORIENTED_EDGE('',*,*,#7365,.F.);
#5401=ORIENTED_EDGE('',*,*,#7366,.T.);
#5402=ORIENTED_EDGE('',*,*,#7360,.T.);
#5403=ORIENTED_EDGE('',*,*,#7367,.T.);
#5404=ORIENTED_EDGE('',*,*,#7368,.F.);
#5405=ORIENTED_EDGE('',*,*,#7369,.T.);
#5406=ORIENTED_EDGE('',*,*,#7370,.T.);
#5407=ORIENTED_EDGE('',*,*,#7365,.T.);
#5408=ORIENTED_EDGE('',*,*,#7371,.F.);
#5409=ORIENTED_EDGE('',*,*,#7368,.T.);
#5410=ORIENTED_EDGE('',*,*,#7372,.T.);
#5411=ORIENTED_EDGE('',*,*,#7363,.F.);
#5412=ORIENTED_EDGE('',*,*,#7373,.F.);
#5413=ORIENTED_EDGE('',*,*,#7371,.T.);
#5414=ORIENTED_EDGE('',*,*,#7374,.T.);
#5415=ORIENTED_EDGE('',*,*,#7343,.T.);
#5416=ORIENTED_EDGE('',*,*,#7375,.T.);
#5417=ORIENTED_EDGE('',*,*,#7357,.T.);
#5418=ORIENTED_EDGE('',*,*,#7376,.T.);
#5419=ORIENTED_EDGE('',*,*,#7329,.T.);
#5420=ORIENTED_EDGE('',*,*,#7377,.T.);
#5421=ORIENTED_EDGE('',*,*,#7378,.T.);
#5422=ORIENTED_EDGE('',*,*,#7328,.F.);
#5423=ORIENTED_EDGE('',*,*,#7379,.F.);
#5424=ORIENTED_EDGE('',*,*,#7347,.F.);
#5425=ORIENTED_EDGE('',*,*,#7352,.F.);
#5426=ORIENTED_EDGE('',*,*,#7356,.F.);
#5427=ORIENTED_EDGE('',*,*,#7380,.F.);
#5428=ORIENTED_EDGE('',*,*,#7333,.F.);
#5429=ORIENTED_EDGE('',*,*,#7338,.F.);
#5430=ORIENTED_EDGE('',*,*,#7342,.F.);
#5431=ORIENTED_EDGE('',*,*,#7381,.F.);
#5432=ORIENTED_EDGE('',*,*,#7361,.F.);
#5433=ORIENTED_EDGE('',*,*,#7366,.F.);
#5434=ORIENTED_EDGE('',*,*,#7370,.F.);
#5435=ORIENTED_EDGE('',*,*,#7382,.F.);
#5436=ORIENTED_EDGE('',*,*,#7319,.F.);
#5437=ORIENTED_EDGE('',*,*,#7324,.F.);
#5438=ORIENTED_EDGE('',*,*,#7383,.F.);
#5439=ORIENTED_EDGE('',*,*,#7364,.T.);
#5440=ORIENTED_EDGE('',*,*,#7384,.T.);
#5441=ORIENTED_EDGE('',*,*,#7336,.F.);
#5442=ORIENTED_EDGE('',*,*,#7385,.T.);
#5443=ORIENTED_EDGE('',*,*,#7350,.F.);
#5444=ORIENTED_EDGE('',*,*,#7386,.T.);
#5445=ORIENTED_EDGE('',*,*,#7322,.F.);
#5446=ORIENTED_EDGE('',*,*,#7387,.T.);
#5447=ORIENTED_EDGE('',*,*,#7372,.F.);
#5448=ORIENTED_EDGE('',*,*,#7388,.F.);
#5449=ORIENTED_EDGE('',*,*,#7330,.F.);
#5450=ORIENTED_EDGE('',*,*,#7389,.F.);
#5451=ORIENTED_EDGE('',*,*,#7358,.F.);
#5452=ORIENTED_EDGE('',*,*,#7390,.F.);
#5453=ORIENTED_EDGE('',*,*,#7344,.F.);
#5454=ORIENTED_EDGE('',*,*,#7391,.F.);
#5455=ORIENTED_EDGE('',*,*,#7392,.T.);
#5456=ORIENTED_EDGE('',*,*,#7334,.F.);
#5457=ORIENTED_EDGE('',*,*,#7380,.T.);
#5458=ORIENTED_EDGE('',*,*,#7355,.F.);
#5459=ORIENTED_EDGE('',*,*,#7375,.F.);
#5460=ORIENTED_EDGE('',*,*,#7341,.F.);
#5461=ORIENTED_EDGE('',*,*,#7374,.F.);
#5462=ORIENTED_EDGE('',*,*,#7362,.F.);
#5463=ORIENTED_EDGE('',*,*,#7381,.T.);
#5464=ORIENTED_EDGE('',*,*,#7327,.F.);
#5465=ORIENTED_EDGE('',*,*,#7376,.F.);
#5466=ORIENTED_EDGE('',*,*,#7348,.F.);
#5467=ORIENTED_EDGE('',*,*,#7379,.T.);
#5468=ORIENTED_EDGE('',*,*,#7331,.F.);
#5469=ORIENTED_EDGE('',*,*,#7390,.T.);
#5470=ORIENTED_EDGE('',*,*,#7353,.F.);
#5471=ORIENTED_EDGE('',*,*,#7385,.F.);
#5472=ORIENTED_EDGE('',*,*,#7339,.F.);
#5473=ORIENTED_EDGE('',*,*,#7384,.F.);
#5474=ORIENTED_EDGE('',*,*,#7359,.F.);
#5475=ORIENTED_EDGE('',*,*,#7391,.T.);
#5476=ORIENTED_EDGE('',*,*,#7325,.F.);
#5477=ORIENTED_EDGE('',*,*,#7386,.F.);
#5478=ORIENTED_EDGE('',*,*,#7345,.F.);
#5479=ORIENTED_EDGE('',*,*,#7389,.T.);
#5480=ORIENTED_EDGE('',*,*,#7373,.T.);
#5481=ORIENTED_EDGE('',*,*,#7392,.F.);
#5482=ORIENTED_EDGE('',*,*,#7388,.T.);
#5483=ORIENTED_EDGE('',*,*,#7367,.F.);
#5484=ORIENTED_EDGE('',*,*,#7387,.F.);
#5485=ORIENTED_EDGE('',*,*,#7317,.F.);
#5486=ORIENTED_EDGE('',*,*,#7393,.F.);
#5487=ORIENTED_EDGE('',*,*,#7383,.T.);
#5488=ORIENTED_EDGE('',*,*,#7378,.F.);
#5489=ORIENTED_EDGE('',*,*,#7393,.T.);
#5490=ORIENTED_EDGE('',*,*,#7377,.F.);
#5491=ORIENTED_EDGE('',*,*,#7320,.F.);
#5492=ORIENTED_EDGE('',*,*,#7382,.T.);
#5493=ORIENTED_EDGE('',*,*,#7369,.F.);
#7317=EDGE_CURVE('',#8678,#8679,#9561,.T.);
#7318=EDGE_CURVE('',#8680,#8679,#9562,.T.);
#7319=EDGE_CURVE('',#8680,#8681,#9563,.T.);
#7320=EDGE_CURVE('',#8681,#8682,#9564,.T.);
#7321=EDGE_CURVE('',#8682,#8678,#9565,.T.);
#7322=EDGE_CURVE('',#8679,#8683,#1009,.T.);
#7323=EDGE_CURVE('',#8684,#8683,#9566,.T.);
#7324=EDGE_CURVE('',#8684,#8680,#1010,.T.);
#7325=EDGE_CURVE('',#8683,#8685,#9567,.T.);
#7326=EDGE_CURVE('',#8686,#8685,#9568,.T.);
#7327=EDGE_CURVE('',#8686,#8687,#9569,.T.);
#7328=EDGE_CURVE('',#8687,#8684,#9570,.T.);
#7329=EDGE_CURVE('',#8686,#8682,#1011,.T.);
#7330=EDGE_CURVE('',#8685,#8678,#1012,.T.);
#7331=EDGE_CURVE('',#8688,#8689,#9571,.T.);
#7332=EDGE_CURVE('',#8690,#8689,#9572,.T.);
#7333=EDGE_CURVE('',#8690,#8691,#9573,.T.);
#7334=EDGE_CURVE('',#8691,#8692,#9574,.T.);
#7335=EDGE_CURVE('',#8692,#8688,#9575,.T.);
#7336=EDGE_CURVE('',#8689,#8693,#1013,.T.);
#7337=EDGE_CURVE('',#8694,#8693,#9576,.T.);
#7338=EDGE_CURVE('',#8694,#8690,#1014,.T.);
#7339=EDGE_CURVE('',#8693,#8695,#9577,.T.);
#7340=EDGE_CURVE('',#8696,#8695,#9578,.T.);
#7341=EDGE_CURVE('',#8696,#8697,#9579,.T.);
#7342=EDGE_CURVE('',#8697,#8694,#9580,.T.);
#7343=EDGE_CURVE('',#8696,#8692,#1015,.T.);
#7344=EDGE_CURVE('',#8695,#8688,#1016,.T.);
#7345=EDGE_CURVE('',#8698,#8699,#9581,.T.);
#7346=EDGE_CURVE('',#8700,#8699,#9582,.T.);
#7347=EDGE_CURVE('',#8700,#8701,#9583,.T.);
#7348=EDGE_CURVE('',#8701,#8702,#9584,.T.);
#7349=EDGE_CURVE('',#8702,#8698,#9585,.T.);
#7350=EDGE_CURVE('',#8699,#8703,#1017,.T.);
#7351=EDGE_CURVE('',#8704,#8703,#9586,.T.);
#7352=EDGE_CURVE('',#8704,#8700,#1018,.T.);
#7353=EDGE_CURVE('',#8703,#8705,#9587,.T.);
#7354=EDGE_CURVE('',#8706,#8705,#9588,.T.);
#7355=EDGE_CURVE('',#8706,#8707,#9589,.T.);
#7356=EDGE_CURVE('',#8707,#8704,#9590,.T.);
#7357=EDGE_CURVE('',#8706,#8702,#1019,.T.);
#7358=EDGE_CURVE('',#8705,#8698,#1020,.T.);
#7359=EDGE_CURVE('',#8708,#8709,#9591,.T.);
#7360=EDGE_CURVE('',#8710,#8709,#9592,.T.);
#7361=EDGE_CURVE('',#8710,#8711,#9593,.T.);
#7362=EDGE_CURVE('',#8711,#8712,#9594,.T.);
#7363=EDGE_CURVE('',#8712,#8708,#9595,.T.);
#7364=EDGE_CURVE('',#8713,#8709,#1021,.T.);
#7365=EDGE_CURVE('',#8714,#8713,#9596,.T.);
#7366=EDGE_CURVE('',#8714,#8710,#1022,.T.);
#7367=EDGE_CURVE('',#8713,#8715,#9597,.T.);
#7368=EDGE_CURVE('',#8716,#8715,#9598,.T.);
#7369=EDGE_CURVE('',#8716,#8717,#9599,.T.);
#7370=EDGE_CURVE('',#8717,#8714,#9600,.T.);
#7371=EDGE_CURVE('',#8716,#8712,#1023,.T.);
#7372=EDGE_CURVE('',#8715,#8708,#1024,.T.);
#7373=EDGE_CURVE('',#8718,#8718,#1025,.T.);
#7374=EDGE_CURVE('',#8712,#8696,#1026,.T.);
#7375=EDGE_CURVE('',#8692,#8706,#1027,.T.);
#7376=EDGE_CURVE('',#8702,#8686,#1028,.T.);
#7377=EDGE_CURVE('',#8682,#8716,#1029,.T.);
#7378=EDGE_CURVE('',#8719,#8719,#1030,.T.);
#7379=EDGE_CURVE('',#8701,#8687,#1031,.T.);
#7380=EDGE_CURVE('',#8691,#8707,#1032,.T.);
#7381=EDGE_CURVE('',#8711,#8697,#1033,.T.);
#7382=EDGE_CURVE('',#8681,#8717,#1034,.T.);
#7383=EDGE_CURVE('',#8720,#8720,#1035,.T.);
#7384=EDGE_CURVE('',#8709,#8693,#1036,.T.);
#7385=EDGE_CURVE('',#8689,#8703,#1037,.T.);
#7386=EDGE_CURVE('',#8699,#8683,#1038,.T.);
#7387=EDGE_CURVE('',#8679,#8713,#1039,.T.);
#7388=EDGE_CURVE('',#8678,#8715,#1040,.T.);
#7389=EDGE_CURVE('',#8698,#8685,#1041,.T.);
#7390=EDGE_CURVE('',#8688,#8705,#1042,.T.);
#7391=EDGE_CURVE('',#8708,#8695,#1043,.T.);
#7392=EDGE_CURVE('',#8721,#8721,#1044,.T.);
#7393=EDGE_CURVE('',#8722,#8722,#1045,.T.);
#8678=VERTEX_POINT('',#41793);
#8679=VERTEX_POINT('',#41794);
#8680=VERTEX_POINT('',#41796);
#8681=VERTEX_POINT('',#41798);
#8682=VERTEX_POINT('',#41800);
#8683=VERTEX_POINT('',#41804);
#8684=VERTEX_POINT('',#41806);
#8685=VERTEX_POINT('',#41810);
#8686=VERTEX_POINT('',#41812);
#8687=VERTEX_POINT('',#41814);
#8688=VERTEX_POINT('',#41821);
#8689=VERTEX_POINT('',#41822);
#8690=VERTEX_POINT('',#41824);
#8691=VERTEX_POINT('',#41826);
#8692=VERTEX_POINT('',#41828);
#8693=VERTEX_POINT('',#41832);
#8694=VERTEX_POINT('',#41834);
#8695=VERTEX_POINT('',#41838);
#8696=VERTEX_POINT('',#41840);
#8697=VERTEX_POINT('',#41842);
#8698=VERTEX_POINT('',#41849);
#8699=VERTEX_POINT('',#41850);
#8700=VERTEX_POINT('',#41852);
#8701=VERTEX_POINT('',#41854);
#8702=VERTEX_POINT('',#41856);
#8703=VERTEX_POINT('',#41860);
#8704=VERTEX_POINT('',#41862);
#8705=VERTEX_POINT('',#41866);
#8706=VERTEX_POINT('',#41868);
#8707=VERTEX_POINT('',#41870);
#8708=VERTEX_POINT('',#41877);
#8709=VERTEX_POINT('',#41878);
#8710=VERTEX_POINT('',#41880);
#8711=VERTEX_POINT('',#41882);
#8712=VERTEX_POINT('',#41884);
#8713=VERTEX_POINT('',#41888);
#8714=VERTEX_POINT('',#41890);
#8715=VERTEX_POINT('',#41894);
#8716=VERTEX_POINT('',#41896);
#8717=VERTEX_POINT('',#41898);
#8718=VERTEX_POINT('',#41905);
#8719=VERTEX_POINT('',#41912);
#8720=VERTEX_POINT('',#41919);
#8721=VERTEX_POINT('',#41930);
#8722=VERTEX_POINT('',#41941);
#9561=LINE('',#41792,#10389);
#9562=LINE('',#41795,#10390);
#9563=LINE('',#41797,#10391);
#9564=LINE('',#41799,#10392);
#9565=LINE('',#41801,#10393);
#9566=LINE('',#41805,#10394);
#9567=LINE('',#41809,#10395);
#9568=LINE('',#41811,#10396);
#9569=LINE('',#41813,#10397);
#9570=LINE('',#41815,#10398);
#9571=LINE('',#41820,#10399);
#9572=LINE('',#41823,#10400);
#9573=LINE('',#41825,#10401);
#9574=LINE('',#41827,#10402);
#9575=LINE('',#41829,#10403);
#9576=LINE('',#41833,#10404);
#9577=LINE('',#41837,#10405);
#9578=LINE('',#41839,#10406);
#9579=LINE('',#41841,#10407);
#9580=LINE('',#41843,#10408);
#9581=LINE('',#41848,#10409);
#9582=LINE('',#41851,#10410);
#9583=LINE('',#41853,#10411);
#9584=LINE('',#41855,#10412);
#9585=LINE('',#41857,#10413);
#9586=LINE('',#41861,#10414);
#9587=LINE('',#41865,#10415);
#9588=LINE('',#41867,#10416);
#9589=LINE('',#41869,#10417);
#9590=LINE('',#41871,#10418);
#9591=LINE('',#41876,#10419);
#9592=LINE('',#41879,#10420);
#9593=LINE('',#41881,#10421);
#9594=LINE('',#41883,#10422);
#9595=LINE('',#41885,#10423);
#9596=LINE('',#41889,#10424);
#9597=LINE('',#41893,#10425);
#9598=LINE('',#41895,#10426);
#9599=LINE('',#41897,#10427);
#9600=LINE('',#41899,#10428);
#10389=VECTOR('',#18861,1.);
#10390=VECTOR('',#18862,1.);
#10391=VECTOR('',#18863,1.);
#10392=VECTOR('',#18864,1.);
#10393=VECTOR('',#18865,1.);
#10394=VECTOR('',#18870,1.);
#10395=VECTOR('',#18875,1.);
#10396=VECTOR('',#18876,1.);
#10397=VECTOR('',#18877,1.);
#10398=VECTOR('',#18878,1.);
#10399=VECTOR('',#18887,1.);
#10400=VECTOR('',#18888,1.);
#10401=VECTOR('',#18889,1.);
#10402=VECTOR('',#18890,1.);
#10403=VECTOR('',#18891,1.);
#10404=VECTOR('',#18896,1.);
#10405=VECTOR('',#18901,1.);
#10406=VECTOR('',#18902,1.);
#10407=VECTOR('',#18903,1.);
#10408=VECTOR('',#18904,1.);
#10409=VECTOR('',#18913,1.);
#10410=VECTOR('',#18914,1.);
#10411=VECTOR('',#18915,1.);
#10412=VECTOR('',#18916,1.);
#10413=VECTOR('',#18917,1.);
#10414=VECTOR('',#18922,1.);
#10415=VECTOR('',#18927,1.);
#10416=VECTOR('',#18928,1.);
#10417=VECTOR('',#18929,1.);
#10418=VECTOR('',#18930,1.);
#10419=VECTOR('',#18939,1.);
#10420=VECTOR('',#18940,1.);
#10421=VECTOR('',#18941,1.);
#10422=VECTOR('',#18942,1.);
#10423=VECTOR('',#18943,1.);
#10424=VECTOR('',#18948,1.);
#10425=VECTOR('',#18953,1.);
#10426=VECTOR('',#18954,1.);
#10427=VECTOR('',#18955,1.);
#10428=VECTOR('',#18956,1.);
#11462=EDGE_LOOP('',(#5340,#5341,#5342,#5343,#5344));
#11463=EDGE_LOOP('',(#5345,#5346,#5347,#5348));
#11464=EDGE_LOOP('',(#5349,#5350,#5351,#5352,#5353));
#11465=EDGE_LOOP('',(#5354,#5355,#5356,#5357));
#11466=EDGE_LOOP('',(#5358,#5359,#5360,#5361,#5362));
#11467=EDGE_LOOP('',(#5363,#5364,#5365,#5366));
#11468=EDGE_LOOP('',(#5367,#5368,#5369,#5370,#5371));
#11469=EDGE_LOOP('',(#5372,#5373,#5374,#5375));
#11470=EDGE_LOOP('',(#5376,#5377,#5378,#5379,#5380));
#11471=EDGE_LOOP('',(#5381,#5382,#5383,#5384));
#11472=EDGE_LOOP('',(#5385,#5386,#5387,#5388,#5389));
#11473=EDGE_LOOP('',(#5390,#5391,#5392,#5393));
#11474=EDGE_LOOP('',(#5394,#5395,#5396,#5397,#5398));
#11475=EDGE_LOOP('',(#5399,#5400,#5401,#5402));
#11476=EDGE_LOOP('',(#5403,#5404,#5405,#5406,#5407));
#11477=EDGE_LOOP('',(#5408,#5409,#5410,#5411));
#11478=EDGE_LOOP('',(#5412));
#11479=EDGE_LOOP('',(#5413,#5414,#5415,#5416,#5417,#5418,#5419,#5420));
#11480=EDGE_LOOP('',(#5421));
#11481=EDGE_LOOP('',(#5422,#5423,#5424,#5425,#5426,#5427,#5428,#5429,#5430,
#5431,#5432,#5433,#5434,#5435,#5436,#5437));
#11482=EDGE_LOOP('',(#5438));
#11483=EDGE_LOOP('',(#5439,#5440,#5441,#5442,#5443,#5444,#5445,#5446));
#11484=EDGE_LOOP('',(#5447,#5448,#5449,#5450,#5451,#5452,#5453,#5454));
#11485=EDGE_LOOP('',(#5455));
#11486=EDGE_LOOP('',(#5456,#5457,#5458,#5459));
#11487=EDGE_LOOP('',(#5460,#5461,#5462,#5463));
#11488=EDGE_LOOP('',(#5464,#5465,#5466,#5467));
#11489=EDGE_LOOP('',(#5468,#5469,#5470,#5471));
#11490=EDGE_LOOP('',(#5472,#5473,#5474,#5475));
#11491=EDGE_LOOP('',(#5476,#5477,#5478,#5479));
#11492=EDGE_LOOP('',(#5480));
#11493=EDGE_LOOP('',(#5481));
#11494=EDGE_LOOP('',(#5482,#5483,#5484,#5485));
#11495=EDGE_LOOP('',(#5486));
#11496=EDGE_LOOP('',(#5487));
#11497=EDGE_LOOP('',(#5488));
#11498=EDGE_LOOP('',(#5489));
#11499=EDGE_LOOP('',(#5490,#5491,#5492,#5493));
#12581=FACE_BOUND('',#11462,.T.);
#12582=FACE_BOUND('',#11463,.T.);
#12583=FACE_BOUND('',#11464,.T.);
#12584=FACE_BOUND('',#11465,.T.);
#12585=FACE_BOUND('',#11466,.T.);
#12586=FACE_BOUND('',#11467,.T.);
#12587=FACE_BOUND('',#11468,.T.);
#12588=FACE_BOUND('',#11469,.T.);
#12589=FACE_BOUND('',#11470,.T.);
#12590=FACE_BOUND('',#11471,.T.);
#12591=FACE_BOUND('',#11472,.T.);
#12592=FACE_BOUND('',#11473,.T.);
#12593=FACE_BOUND('',#11474,.T.);
#12594=FACE_BOUND('',#11475,.T.);
#12595=FACE_BOUND('',#11476,.T.);
#12596=FACE_BOUND('',#11477,.T.);
#12597=FACE_BOUND('',#11478,.T.);
#12598=FACE_BOUND('',#11479,.T.);
#12599=FACE_BOUND('',#11480,.T.);
#12600=FACE_BOUND('',#11481,.T.);
#12601=FACE_BOUND('',#11482,.T.);
#12602=FACE_BOUND('',#11483,.T.);
#12603=FACE_BOUND('',#11484,.T.);
#12604=FACE_BOUND('',#11485,.T.);
#12605=FACE_BOUND('',#11486,.T.);
#12606=FACE_BOUND('',#11487,.T.);
#12607=FACE_BOUND('',#11488,.T.);
#12608=FACE_BOUND('',#11489,.T.);
#12609=FACE_BOUND('',#11490,.T.);
#12610=FACE_BOUND('',#11491,.T.);
#12611=FACE_BOUND('',#11492,.T.);
#12612=FACE_BOUND('',#11493,.T.);
#12613=FACE_BOUND('',#11494,.T.);
#12614=FACE_BOUND('',#11495,.T.);
#12615=FACE_BOUND('',#11496,.T.);
#12616=FACE_BOUND('',#11497,.T.);
#12617=FACE_BOUND('',#11498,.T.);
#12618=FACE_BOUND('',#11499,.T.);
#13440=ADVANCED_FACE('',(#12581),#1523,.F.);
#13441=ADVANCED_FACE('',(#12582),#1809,.F.);
#13442=ADVANCED_FACE('',(#12583),#1524,.F.);
#13443=ADVANCED_FACE('',(#12584),#1810,.T.);
#13444=ADVANCED_FACE('',(#12585),#1525,.T.);
#13445=ADVANCED_FACE('',(#12586),#1811,.F.);
#13446=ADVANCED_FACE('',(#12587),#1526,.T.);
#13447=ADVANCED_FACE('',(#12588),#1812,.T.);
#13448=ADVANCED_FACE('',(#12589),#1527,.F.);
#13449=ADVANCED_FACE('',(#12590),#1813,.F.);
#13450=ADVANCED_FACE('',(#12591),#1528,.T.);
#13451=ADVANCED_FACE('',(#12592),#1814,.T.);
#13452=ADVANCED_FACE('',(#12593),#1529,.T.);
#13453=ADVANCED_FACE('',(#12594),#1815,.F.);
#13454=ADVANCED_FACE('',(#12595),#1530,.F.);
#13455=ADVANCED_FACE('',(#12596),#1816,.T.);
#13456=ADVANCED_FACE('',(#12597,#12598),#1531,.T.);
#13457=ADVANCED_FACE('',(#12599,#12600),#1532,.T.);
#13458=ADVANCED_FACE('',(#12601,#12602),#1533,.T.);
#13459=ADVANCED_FACE('',(#12603,#12604),#1534,.T.);
#13460=ADVANCED_FACE('',(#12605),#32,.F.);
#13461=ADVANCED_FACE('',(#12606),#33,.F.);
#13462=ADVANCED_FACE('',(#12607),#34,.F.);
#13463=ADVANCED_FACE('',(#12608),#35,.T.);
#13464=ADVANCED_FACE('',(#12609),#36,.T.);
#13465=ADVANCED_FACE('',(#12610),#37,.T.);
#13466=ADVANCED_FACE('',(#12611,#12612),#1817,.F.);
#13467=ADVANCED_FACE('',(#12613),#38,.T.);
#13468=ADVANCED_FACE('',(#12614,#12615),#1818,.T.);
#13469=ADVANCED_FACE('',(#12616,#12617),#331,.T.);
#13470=ADVANCED_FACE('',(#12618),#39,.F.);
#13526=CLOSED_SHELL('',(#13440,#13441,#13442,#13443,#13444,#13445,#13446,
#13447,#13448,#13449,#13450,#13451,#13452,#13453,#13454,#13455,#13456,#13457,
#13458,#13459,#13460,#13461,#13462,#13463,#13464,#13465,#13466,#13467,#13468,
#13469,#13470));
#13553=STYLED_ITEM('',(#13580),#13743);
#13580=PRESENTATION_STYLE_ASSIGNMENT((#13607));
#13607=SURFACE_STYLE_USAGE(.BOTH.,#13634);
#13634=SURFACE_SIDE_STYLE('',(#13661));
#13661=SURFACE_STYLE_FILL_AREA(#13688);
#13688=FILL_AREA_STYLE('',(#13715));
#13715=FILL_AREA_STYLE_COLOUR('',#60);
#13743=MANIFOLD_SOLID_BREP('ball_retainer',#13526);
#13771=SHAPE_DEFINITION_REPRESENTATION(#45579,#13799);
#13799=SHAPE_REPRESENTATION('ball_retainer',(#13802),#45489);
#13802=AXIS2_PLACEMENT_3D('',#19109,#15295,#15296);
#15190=AXIS2_PLACEMENT_3D('',#41791,#18859,#18860);
#15191=AXIS2_PLACEMENT_3D('',#41802,#18866,#18867);
#15192=AXIS2_PLACEMENT_3D('',#41803,#18868,#18869);
#15193=AXIS2_PLACEMENT_3D('',#41807,#18871,#18872);
#15194=AXIS2_PLACEMENT_3D('',#41808,#18873,#18874);
#15195=AXIS2_PLACEMENT_3D('',#41816,#18879,#18880);
#15196=AXIS2_PLACEMENT_3D('',#41817,#18881,#18882);
#15197=AXIS2_PLACEMENT_3D('',#41818,#18883,#18884);
#15198=AXIS2_PLACEMENT_3D('',#41819,#18885,#18886);
#15199=AXIS2_PLACEMENT_3D('',#41830,#18892,#18893);
#15200=AXIS2_PLACEMENT_3D('',#41831,#18894,#18895);
#15201=AXIS2_PLACEMENT_3D('',#41835,#18897,#18898);
#15202=AXIS2_PLACEMENT_3D('',#41836,#18899,#18900);
#15203=AXIS2_PLACEMENT_3D('',#41844,#18905,#18906);
#15204=AXIS2_PLACEMENT_3D('',#41845,#18907,#18908);
#15205=AXIS2_PLACEMENT_3D('',#41846,#18909,#18910);
#15206=AXIS2_PLACEMENT_3D('',#41847,#18911,#18912);
#15207=AXIS2_PLACEMENT_3D('',#41858,#18918,#18919);
#15208=AXIS2_PLACEMENT_3D('',#41859,#18920,#18921);
#15209=AXIS2_PLACEMENT_3D('',#41863,#18923,#18924);
#15210=AXIS2_PLACEMENT_3D('',#41864,#18925,#18926);
#15211=AXIS2_PLACEMENT_3D('',#41872,#18931,#18932);
#15212=AXIS2_PLACEMENT_3D('',#41873,#18933,#18934);
#15213=AXIS2_PLACEMENT_3D('',#41874,#18935,#18936);
#15214=AXIS2_PLACEMENT_3D('',#41875,#18937,#18938);
#15215=AXIS2_PLACEMENT_3D('',#41886,#18944,#18945);
#15216=AXIS2_PLACEMENT_3D('',#41887,#18946,#18947);
#15217=AXIS2_PLACEMENT_3D('',#41891,#18949,#18950);
#15218=AXIS2_PLACEMENT_3D('',#41892,#18951,#18952);
#15219=AXIS2_PLACEMENT_3D('',#41900,#18957,#18958);
#15220=AXIS2_PLACEMENT_3D('',#41901,#18959,#18960);
#15221=AXIS2_PLACEMENT_3D('',#41902,#18961,#18962);
#15222=AXIS2_PLACEMENT_3D('',#41903,#18963,#18964);
#15223=AXIS2_PLACEMENT_3D('',#41904,#18965,#18966);
#15224=AXIS2_PLACEMENT_3D('',#41906,#18967,#18968);
#15225=AXIS2_PLACEMENT_3D('',#41907,#18969,#18970);
#15226=AXIS2_PLACEMENT_3D('',#41908,#18971,#18972);
#15227=AXIS2_PLACEMENT_3D('',#41909,#18973,#18974);
#15228=AXIS2_PLACEMENT_3D('',#41910,#18975,#18976);
#15229=AXIS2_PLACEMENT_3D('',#41911,#18977,#18978);
#15230=AXIS2_PLACEMENT_3D('',#41913,#18979,#18980);
#15231=AXIS2_PLACEMENT_3D('',#41914,#18981,#18982);
#15232=AXIS2_PLACEMENT_3D('',#41915,#18983,#18984);
#15233=AXIS2_PLACEMENT_3D('',#41916,#18985,#18986);
#15234=AXIS2_PLACEMENT_3D('',#41917,#18987,#18988);
#15235=AXIS2_PLACEMENT_3D('',#41918,#18989,#18990);
#15236=AXIS2_PLACEMENT_3D('',#41920,#18991,#18992);
#15237=AXIS2_PLACEMENT_3D('',#41921,#18993,#18994);
#15238=AXIS2_PLACEMENT_3D('',#41922,#18995,#18996);
#15239=AXIS2_PLACEMENT_3D('',#41923,#18997,#18998);
#15240=AXIS2_PLACEMENT_3D('',#41924,#18999,#19000);
#15241=AXIS2_PLACEMENT_3D('',#41925,#19001,#19002);
#15242=AXIS2_PLACEMENT_3D('',#41926,#19003,#19004);
#15243=AXIS2_PLACEMENT_3D('',#41927,#19005,#19006);
#15244=AXIS2_PLACEMENT_3D('',#41928,#19007,#19008);
#15245=AXIS2_PLACEMENT_3D('',#41929,#19009,#19010);
#15246=AXIS2_PLACEMENT_3D('',#41931,#19011,#19012);
#15247=AXIS2_PLACEMENT_3D('',#41932,#19013,#19014);
#15248=AXIS2_PLACEMENT_3D('',#41933,#19015,#19016);
#15249=AXIS2_PLACEMENT_3D('',#41934,#19017,#19018);
#15250=AXIS2_PLACEMENT_3D('',#41935,#19019,#19020);
#15251=AXIS2_PLACEMENT_3D('',#41936,#19021,#19022);
#15252=AXIS2_PLACEMENT_3D('',#41937,#19023,#19024);
#15253=AXIS2_PLACEMENT_3D('',#41938,#19025,#19026);
#15254=AXIS2_PLACEMENT_3D('',#41939,#19027,#19028);
#15255=AXIS2_PLACEMENT_3D('',#41940,#19029,#19030);
#15256=AXIS2_PLACEMENT_3D('',#41942,#19031,#19032);
#15257=AXIS2_PLACEMENT_3D('',#41943,#19033,#19034);
#15295=DIRECTION('',(0.,0.,1.));
#15296=DIRECTION('',(1.,0.,0.));
#18859=DIRECTION('',(-0.173648177666933,0.984807753012207,0.));
#18860=DIRECTION('',(-0.984807753012207,-0.173648177666933,0.));
#18861=DIRECTION('',(-0.463976173764915,-0.0818115178406352,-0.882061781128216));
#18862=DIRECTION('',(0.,0.,1.));
#18863=DIRECTION('',(0.984807753012207,0.173648177666933,0.));
#18864=DIRECTION('',(0.463976173764915,0.0818115178406351,0.882061781128216));
#18865=DIRECTION('',(0.,0.,1.));
#18866=DIRECTION('',(0.,0.,1.));
#18867=DIRECTION('',(1.,0.,0.));
#18868=DIRECTION('',(0.,0.,1.));
#18869=DIRECTION('',(1.,0.,0.));
#18870=DIRECTION('',(0.,0.,1.));
#18871=DIRECTION('',(0.,0.,-1.));
#18872=DIRECTION('',(-1.,0.,0.));
#18873=DIRECTION('',(0.98480775301221,-0.17364817766692,0.));
#18874=DIRECTION('',(0.17364817766692,0.98480775301221,0.));
#18875=DIRECTION('',(0.0818115178406285,0.463976173764916,0.882061781128216));
#18876=DIRECTION('',(0.,0.,1.));
#18877=DIRECTION('',(-0.0818115178406284,-0.463976173764916,-0.882061781128216));
#18878=DIRECTION('',(-0.17364817766692,-0.98480775301221,0.));
#18879=DIRECTION('',(0.,0.,1.));
#18880=DIRECTION('',(1.,0.,0.));
#18881=DIRECTION('',(0.,0.,-1.));
#18882=DIRECTION('',(-1.,0.,0.));
#18883=DIRECTION('',(0.,0.,-1.));
#18884=DIRECTION('',(1.,0.,0.));
#18885=DIRECTION('',(-0.173648177666933,0.984807753012207,0.));
#18886=DIRECTION('',(-0.984807753012207,-0.173648177666933,0.));
#18887=DIRECTION('',(0.463976173764915,0.0818115178406386,-0.882061781128216));
#18888=DIRECTION('',(0.,0.,1.));
#18889=DIRECTION('',(-0.984807753012206,-0.173648177666941,0.));
#18890=DIRECTION('',(-0.463976173764914,-0.0818115178406385,0.882061781128216));
#18891=DIRECTION('',(0.,0.,1.));
#18892=DIRECTION('',(0.,0.,1.));
#18893=DIRECTION('',(1.,0.,0.));
#18894=DIRECTION('',(0.,0.,1.));
#18895=DIRECTION('',(1.,0.,0.));
#18896=DIRECTION('',(0.,0.,1.));
#18897=DIRECTION('',(0.,0.,-1.));
#18898=DIRECTION('',(-1.,0.,0.));
#18899=DIRECTION('',(0.98480775301221,-0.17364817766692,0.));
#18900=DIRECTION('',(0.17364817766692,0.98480775301221,0.));
#18901=DIRECTION('',(-0.0818115178406318,-0.463976173764916,0.882061781128216));
#18902=DIRECTION('',(0.,0.,1.));
#18903=DIRECTION('',(0.0818115178406318,0.463976173764915,-0.882061781128216));
#18904=DIRECTION('',(0.173648177666927,0.984807753012209,0.));
#18905=DIRECTION('',(0.,0.,1.));
#18906=DIRECTION('',(1.,0.,0.));
#18907=DIRECTION('',(0.,0.,-1.));
#18908=DIRECTION('',(-1.,0.,0.));
#18909=DIRECTION('',(0.,0.,-1.));
#18910=DIRECTION('',(1.,0.,0.));
#18911=DIRECTION('',(-0.984807753012206,-0.173648177666945,0.));
#18912=DIRECTION('',(0.173648177666945,-0.984807753012206,0.));
#18913=DIRECTION('',(0.0818115178406402,-0.463976173764914,-0.882061781128216));
#18914=DIRECTION('',(0.,0.,1.));
#18915=DIRECTION('',(-0.173648177666945,0.984807753012206,0.));
#18916=DIRECTION('',(-0.0818115178406402,0.463976173764914,0.882061781128216));
#18917=DIRECTION('',(0.,0.,1.));
#18918=DIRECTION('',(0.,0.,1.));
#18919=DIRECTION('',(1.,0.,0.));
#18920=DIRECTION('',(0.,0.,1.));
#18921=DIRECTION('',(1.,0.,0.));
#18922=DIRECTION('',(0.,0.,1.));
#18923=DIRECTION('',(0.,0.,-1.));
#18924=DIRECTION('',(-1.,0.,0.));
#18925=DIRECTION('',(-0.17364817766693,-0.984807753012208,0.));
#18926=DIRECTION('',(0.984807753012208,-0.17364817766693,0.));
#18927=DIRECTION('',(-0.463976173764916,0.0818115178406334,0.882061781128216));
#18928=DIRECTION('',(0.,0.,1.));
#18929=DIRECTION('',(0.463976173764915,-0.0818115178406334,-0.882061781128216));
#18930=DIRECTION('',(0.984807753012208,-0.17364817766693,0.));
#18931=DIRECTION('',(0.,0.,1.));
#18932=DIRECTION('',(1.,0.,0.));
#18933=DIRECTION('',(0.,0.,-1.));
#18934=DIRECTION('',(-1.,0.,0.));
#18935=DIRECTION('',(0.,0.,-1.));
#18936=DIRECTION('',(1.,0.,0.));
#18937=DIRECTION('',(-0.984807753012206,-0.173648177666945,0.));
#18938=DIRECTION('',(0.173648177666945,-0.984807753012206,0.));
#18939=DIRECTION('',(-0.0818115178406369,0.463976173764915,-0.882061781128216));
#18940=DIRECTION('',(0.,0.,1.));
#18941=DIRECTION('',(0.173648177666938,-0.984807753012207,0.));
#18942=DIRECTION('',(0.0818115178406368,-0.463976173764915,0.882061781128216));
#18943=DIRECTION('',(0.,0.,1.));
#18944=DIRECTION('',(0.,0.,1.));
#18945=DIRECTION('',(1.,0.,0.));
#18946=DIRECTION('',(0.,0.,-1.));
#18947=DIRECTION('',(-1.,0.,0.));
#18948=DIRECTION('',(0.,0.,1.));
#18949=DIRECTION('',(0.,0.,-1.));
#18950=DIRECTION('',(-1.,0.,0.));
#18951=DIRECTION('',(-0.17364817766693,-0.984807753012208,0.));
#18952=DIRECTION('',(0.984807753012208,-0.17364817766693,0.));
#18953=DIRECTION('',(0.463976173764916,-0.0818115178406335,0.882061781128216));
#18954=DIRECTION('',(0.,0.,1.));
#18955=DIRECTION('',(-0.463976173764915,0.0818115178406334,-0.882061781128216));
#18956=DIRECTION('',(-0.984807753012208,0.17364817766693,0.));
#18957=DIRECTION('',(0.,0.,1.));
#18958=DIRECTION('',(1.,0.,0.));
#18959=DIRECTION('',(0.,0.,-1.));
#18960=DIRECTION('',(-1.,0.,0.));
#18961=DIRECTION('',(0.,0.,-1.));
#18962=DIRECTION('',(-1.,0.,0.));
#18963=DIRECTION('',(0.,0.,-1.));
#18964=DIRECTION('',(-1.,0.,0.));
#18965=DIRECTION('',(0.,0.,-1.));
#18966=DIRECTION('',(-1.,0.,0.));
#18967=DIRECTION('',(0.,0.,-1.));
#18968=DIRECTION('',(-1.,0.,0.));
#18969=DIRECTION('',(0.,0.,-1.));
#18970=DIRECTION('',(-1.,0.,0.));
#18971=DIRECTION('',(0.,0.,-1.));
#18972=DIRECTION('',(-1.,0.,0.));
#18973=DIRECTION('',(0.,0.,-1.));
#18974=DIRECTION('',(-1.,0.,0.));
#18975=DIRECTION('',(0.,0.,-1.));
#18976=DIRECTION('',(-1.,0.,0.));
#18977=DIRECTION('',(0.,0.,-1.));
#18978=DIRECTION('',(-1.,0.,0.));
#18979=DIRECTION('',(0.,0.,-1.));
#18980=DIRECTION('',(-1.,0.,0.));
#18981=DIRECTION('',(0.,0.,-1.));
#18982=DIRECTION('',(-1.,0.,0.));
#18983=DIRECTION('',(0.,0.,-1.));
#18984=DIRECTION('',(-1.,0.,0.));
#18985=DIRECTION('',(0.,0.,-1.));
#18986=DIRECTION('',(-1.,0.,0.));
#18987=DIRECTION('',(0.,0.,1.));
#18988=DIRECTION('',(1.,0.,0.));
#18989=DIRECTION('',(0.,0.,-1.));
#18990=DIRECTION('',(-1.,0.,0.));
#18991=DIRECTION('',(0.,0.,-1.));
#18992=DIRECTION('',(-1.,0.,0.));
#18993=DIRECTION('',(0.,0.,-1.));
#18994=DIRECTION('',(-1.,0.,0.));
#18995=DIRECTION('',(0.,0.,-1.));
#18996=DIRECTION('',(-1.,0.,0.));
#18997=DIRECTION('',(0.,0.,-1.));
#18998=DIRECTION('',(-1.,0.,0.));
#18999=DIRECTION('',(0.,0.,1.));
#19000=DIRECTION('',(1.,0.,0.));
#19001=DIRECTION('',(0.,0.,-1.));
#19002=DIRECTION('',(-1.,0.,0.));
#19003=DIRECTION('',(0.,0.,-1.));
#19004=DIRECTION('',(-1.,0.,0.));
#19005=DIRECTION('',(0.,0.,-1.));
#19006=DIRECTION('',(-1.,0.,0.));
#19007=DIRECTION('',(0.,0.,-1.));
#19008=DIRECTION('',(-1.,0.,0.));
#19009=DIRECTION('',(0.,0.,-1.));
#19010=DIRECTION('',(-1.,0.,0.));
#19011=DIRECTION('',(0.,0.,-1.));
#19012=DIRECTION('',(-1.,0.,0.));
#19013=DIRECTION('',(0.,0.,-1.));
#19014=DIRECTION('',(-1.,0.,0.));
#19015=DIRECTION('',(0.,0.,-1.));
#19016=DIRECTION('',(-1.,0.,0.));
#19017=DIRECTION('',(0.,0.,-1.));
#19018=DIRECTION('',(-1.,0.,0.));
#19019=DIRECTION('',(0.,0.,-1.));
#19020=DIRECTION('',(-1.,0.,0.));
#19021=DIRECTION('',(0.,0.,-1.));
#19022=DIRECTION('',(-1.,0.,0.));
#19023=DIRECTION('',(0.,0.,-1.));
#19024=DIRECTION('',(-1.,0.,0.));
#19025=DIRECTION('',(0.,0.,-1.));
#19026=DIRECTION('',(-1.,0.,0.));
#19027=DIRECTION('',(0.,0.,-1.));
#19028=DIRECTION('',(-1.,0.,0.));
#19029=DIRECTION('',(0.,0.,-1.));
#19030=DIRECTION('',(-1.,0.,0.));
#19031=DIRECTION('',(0.,0.,-1.));
#19032=DIRECTION('',(-1.,0.,0.));
#19033=DIRECTION('',(0.,0.,-1.));
#19034=DIRECTION('',(-1.,0.,0.));
#19109=CARTESIAN_POINT('',(0.,0.,0.));
#41791=CARTESIAN_POINT('',(-0.00295442325903663,-0.000520944533000792,-0.0210189377942895));
#41792=CARTESIAN_POINT('',(-1.61911969068189E-18,9.18248406554907E-18,-0.00540230489496124));
#41793=CARTESIAN_POINT('',(-0.00295442325903663,-0.000520944533000792,-0.0110189377942895));
#41794=CARTESIAN_POINT('',(-0.00590884651807325,-0.00104188906600159,-0.0166355706936178));
#41795=CARTESIAN_POINT('',(-0.00590884651807325,-0.00104188906600159,-0.0210189377942895));
#41796=CARTESIAN_POINT('',(-0.00590884651807325,-0.00104188906600159,-0.0176355706936178));
#41797=CARTESIAN_POINT('',(-0.00746781659002574,-0.00131677755180384,-0.0176355706936178));
#41798=CARTESIAN_POINT('',(-0.00433080680353718,-0.000763638087699395,-0.0176355706936178));
#41799=CARTESIAN_POINT('',(-1.61911969068189E-18,9.18248406554907E-18,-0.00940230489496124));
#41800=CARTESIAN_POINT('',(-0.00295442325903663,-0.000520944533000792,-0.0150189377942895));
#41801=CARTESIAN_POINT('',(-0.00295442325903663,-0.000520944533000792,-0.0210189377942895));
#41802=CARTESIAN_POINT('',(0.,0.,-0.0210189377942895));
#41803=CARTESIAN_POINT('',(0.,0.,-0.0166355706936178));
#41804=CARTESIAN_POINT('',(-0.00104188906600158,-0.00590884651807325,-0.0166355706936178));
#41805=CARTESIAN_POINT('',(-0.00104188906600158,-0.00590884651807325,-0.0210189377942895));
#41806=CARTESIAN_POINT('',(-0.00104188906600158,-0.00590884651807325,-0.0176355706936178));
#41807=CARTESIAN_POINT('',(0.,0.,-0.0176355706936178));
#41808=CARTESIAN_POINT('',(-0.000520944533000823,-0.00295442325903662,-0.0210189377942895));
#41809=CARTESIAN_POINT('',(-6.4490934599903E-17,1.13714917810672E-17,-0.00540230489496124));
#41810=CARTESIAN_POINT('',(-0.000520944533000823,-0.00295442325903662,-0.0110189377942895));
#41811=CARTESIAN_POINT('',(-0.000520944533000823,-0.00295442325903662,-0.0210189377942895));
#41812=CARTESIAN_POINT('',(-0.000520944533000823,-0.00295442325903662,-0.0150189377942895));
#41813=CARTESIAN_POINT('',(-6.4490934599903E-17,1.13714917810672E-17,-0.00940230489496124));
#41814=CARTESIAN_POINT('',(-0.000763638087699406,-0.00433080680353718,-0.0176355706936178));
#41815=CARTESIAN_POINT('',(-0.000232183409974289,-0.00131677755180373,-0.0176355706936178));
#41816=CARTESIAN_POINT('',(0.,0.,-0.0210189377942895));
#41817=CARTESIAN_POINT('',(0.,0.,-0.0150189377942895));
#41818=CARTESIAN_POINT('',(0.,0.,-0.0110189377942895));
#41819=CARTESIAN_POINT('',(-0.00295442325903663,-0.000520944533000792,-0.0210189377942895));
#41820=CARTESIAN_POINT('',(8.99929316448808E-18,-5.1037527713168E-17,-0.00540230489496124));
#41821=CARTESIAN_POINT('',(0.00295442325903663,0.000520944533000772,-0.0110189377942895));
#41822=CARTESIAN_POINT('',(0.00590884651807325,0.00104188906600159,-0.0166355706936178));
#41823=CARTESIAN_POINT('',(0.00590884651807325,0.00104188906600159,-0.0210189377942895));
#41824=CARTESIAN_POINT('',(0.00590884651807325,0.00104188906600159,-0.0176355706936178));
#41825=CARTESIAN_POINT('',(-0.00746781659002571,-0.00131677755180395,-0.0176355706936178));
#41826=CARTESIAN_POINT('',(0.00433080680353718,0.000763638087699384,-0.0176355706936178));
#41827=CARTESIAN_POINT('',(8.99929316448808E-18,-5.1037527713168E-17,-0.00940230489496124));
#41828=CARTESIAN_POINT('',(0.00295442325903663,0.000520944533000771,-0.0150189377942895));
#41829=CARTESIAN_POINT('',(0.00295442325903663,0.000520944533000771,-0.0210189377942895));
#41830=CARTESIAN_POINT('',(0.,0.,-0.0210189377942895));
#41831=CARTESIAN_POINT('',(0.,0.,-0.0166355706936178));
#41832=CARTESIAN_POINT('',(0.00104188906600158,0.00590884651807325,-0.0166355706936178));
#41833=CARTESIAN_POINT('',(0.00104188906600158,0.00590884651807325,-0.0210189377942895));
#41834=CARTESIAN_POINT('',(0.00104188906600158,0.00590884651807325,-0.0176355706936178));
#41835=CARTESIAN_POINT('',(0.,0.,-0.0176355706936178));
#41836=CARTESIAN_POINT('',(-0.000520944533000823,-0.00295442325903662,-0.0210189377942895));
#41837=CARTESIAN_POINT('',(2.25291178817541E-17,-3.9724913341147E-18,-0.00540230489496124));
#41838=CARTESIAN_POINT('',(0.000520944533000802,0.00295442325903663,-0.0110189377942895));
#41839=CARTESIAN_POINT('',(0.000520944533000802,0.00295442325903663,-0.0210189377942895));
#41840=CARTESIAN_POINT('',(0.000520944533000802,0.00295442325903663,-0.0150189377942895));
#41841=CARTESIAN_POINT('',(2.25291178817541E-17,-3.9724913341147E-18,-0.00940230489496124));
#41842=CARTESIAN_POINT('',(0.000763638087699395,0.00433080680353718,-0.0176355706936178));
#41843=CARTESIAN_POINT('',(-0.000232183409974221,-0.0013167775518038,-0.0176355706936178));
#41844=CARTESIAN_POINT('',(0.,0.,-0.0210189377942895));
#41845=CARTESIAN_POINT('',(0.,0.,-0.0150189377942895));
#41846=CARTESIAN_POINT('',(0.,0.,-0.0110189377942895));
#41847=CARTESIAN_POINT('',(0.000520944533000761,-0.00295442325903663,-0.0210189377942895));
#41848=CARTESIAN_POINT('',(-7.21785956780367E-17,-1.27270338476863E-17,
-0.00540230489496124));
#41849=CARTESIAN_POINT('',(0.000520944533000761,-0.00295442325903663,-0.0110189377942895));
#41850=CARTESIAN_POINT('',(0.00104188906600159,-0.00590884651807325,-0.0166355706936178));
#41851=CARTESIAN_POINT('',(0.00104188906600159,-0.00590884651807325,-0.0210189377942895));
#41852=CARTESIAN_POINT('',(0.00104188906600159,-0.00590884651807325,-0.0176355706936178));
#41853=CARTESIAN_POINT('',(-0.000232183409974364,0.00131677755180391,-0.0176355706936178));
#41854=CARTESIAN_POINT('',(0.000763638087699379,-0.00433080680353719,-0.0176355706936178));
#41855=CARTESIAN_POINT('',(-7.21785956780367E-17,-1.27270338476863E-17,
-0.00940230489496124));
#41856=CARTESIAN_POINT('',(0.000520944533000761,-0.00295442325903663,-0.0150189377942895));
#41857=CARTESIAN_POINT('',(0.000520944533000761,-0.00295442325903663,-0.0210189377942895));
#41858=CARTESIAN_POINT('',(0.,0.,-0.0210189377942895));
#41859=CARTESIAN_POINT('',(0.,0.,-0.0166355706936178));
#41860=CARTESIAN_POINT('',(0.00590884651807325,-0.00104188906600158,-0.0166355706936178));
#41861=CARTESIAN_POINT('',(0.00590884651807325,-0.00104188906600158,-0.0210189377942895));
#41862=CARTESIAN_POINT('',(0.00590884651807325,-0.00104188906600158,-0.0176355706936178));
#41863=CARTESIAN_POINT('',(0.,0.,-0.0176355706936178));
#41864=CARTESIAN_POINT('',(-0.00295442325903663,0.000520944533000792,-0.0210189377942895));
#41865=CARTESIAN_POINT('',(-3.76539462949268E-19,-2.13546141059281E-18,
-0.00540230489496124));
#41866=CARTESIAN_POINT('',(0.00295442325903663,-0.000520944533000792,-0.0110189377942895));
#41867=CARTESIAN_POINT('',(0.00295442325903663,-0.000520944533000792,-0.0210189377942895));
#41868=CARTESIAN_POINT('',(0.00295442325903663,-0.000520944533000792,-0.0150189377942895));
#41869=CARTESIAN_POINT('',(-3.76539462949268E-19,-2.13546141059281E-18,
-0.00940230489496124));
#41870=CARTESIAN_POINT('',(0.00433080680353719,-0.00076363808769939,-0.0176355706936178));
#41871=CARTESIAN_POINT('',(-0.00746781659002575,0.00131677755180382,-0.0176355706936178));
#41872=CARTESIAN_POINT('',(0.,0.,-0.0210189377942895));
#41873=CARTESIAN_POINT('',(0.,0.,-0.0150189377942895));
#41874=CARTESIAN_POINT('',(0.,0.,-0.0110189377942895));
#41875=CARTESIAN_POINT('',(0.000520944533000761,-0.00295442325903663,-0.0210189377942895));
#41876=CARTESIAN_POINT('',(3.02167789598882E-17,5.32803340073238E-18,-0.00540230489496124));
#41877=CARTESIAN_POINT('',(-0.000520944533000782,0.00295442325903663,-0.0110189377942895));
#41878=CARTESIAN_POINT('',(-0.00104188906600159,0.00590884651807325,-0.0166355706936178));
#41879=CARTESIAN_POINT('',(-0.00104188906600159,0.00590884651807325,-0.0210189377942895));
#41880=CARTESIAN_POINT('',(-0.00104188906600159,0.00590884651807325,-0.0176355706936178));
#41881=CARTESIAN_POINT('',(-0.00023218340997424,0.00131677755180388,-0.0176355706936178));
#41882=CARTESIAN_POINT('',(-0.000763638087699389,0.00433080680353718,-0.0176355706936178));
#41883=CARTESIAN_POINT('',(3.02167789598882E-17,5.32803340073238E-18,-0.00940230489496124));
#41884=CARTESIAN_POINT('',(-0.000520944533000782,0.00295442325903663,-0.0150189377942895));
#41885=CARTESIAN_POINT('',(-0.000520944533000782,0.00295442325903663,-0.0210189377942895));
#41886=CARTESIAN_POINT('',(0.,0.,-0.0210189377942895));
#41887=CARTESIAN_POINT('',(0.,0.,-0.0166355706936178));
#41888=CARTESIAN_POINT('',(-0.00590884651807325,0.00104188906600158,-0.0166355706936178));
#41889=CARTESIAN_POINT('',(-0.00590884651807325,0.00104188906600158,-0.0210189377942895));
#41890=CARTESIAN_POINT('',(-0.00590884651807325,0.00104188906600158,-0.0176355706936178));
#41891=CARTESIAN_POINT('',(0.,0.,-0.0176355706936178));
#41892=CARTESIAN_POINT('',(-0.00295442325903663,0.000520944533000792,-0.0210189377942895));
#41893=CARTESIAN_POINT('',(3.76539462949268E-19,2.13546141059281E-18,-0.00540230489496124));
#41894=CARTESIAN_POINT('',(-0.00295442325903663,0.000520944533000792,-0.0110189377942895));
#41895=CARTESIAN_POINT('',(-0.00295442325903663,0.000520944533000792,-0.0210189377942895));
#41896=CARTESIAN_POINT('',(-0.00295442325903663,0.000520944533000792,-0.0150189377942895));
#41897=CARTESIAN_POINT('',(3.76539462949268E-19,2.13546141059281E-18,-0.00940230489496124));
#41898=CARTESIAN_POINT('',(-0.00433080680353719,0.00076363808769939,-0.0176355706936178));
#41899=CARTESIAN_POINT('',(-0.00746781659002575,0.00131677755180382,-0.0176355706936178));
#41900=CARTESIAN_POINT('',(0.,0.,-0.0210189377942895));
#41901=CARTESIAN_POINT('',(0.,0.,-0.0150189377942895));
#41902=CARTESIAN_POINT('',(0.,0.,-0.0110189377942895));
#41903=CARTESIAN_POINT('',(-0.00180420299878392,0.,-0.0150189377942895));
#41904=CARTESIAN_POINT('',(0.,0.,-0.0150189377942895));
#41905=CARTESIAN_POINT('',(-0.00180420299878392,0.,-0.0150189377942895));
#41906=CARTESIAN_POINT('',(0.,0.,-0.0150189377942895));
#41907=CARTESIAN_POINT('',(0.,0.,-0.0150189377942895));
#41908=CARTESIAN_POINT('',(0.,0.,-0.0150189377942895));
#41909=CARTESIAN_POINT('',(0.,0.,-0.0150189377942895));
#41910=CARTESIAN_POINT('',(-0.0077,0.,-0.0176355706936178));
#41911=CARTESIAN_POINT('',(0.,0.,-0.0176355706936178));
#41912=CARTESIAN_POINT('',(-0.0077,0.,-0.0176355706936178));
#41913=CARTESIAN_POINT('',(0.,0.,-0.0176355706936178));
#41914=CARTESIAN_POINT('',(0.,0.,-0.0176355706936178));
#41915=CARTESIAN_POINT('',(0.,0.,-0.0176355706936178));
#41916=CARTESIAN_POINT('',(0.,0.,-0.0176355706936178));
#41917=CARTESIAN_POINT('',(-0.008,0.,-0.0166355706936178));
#41918=CARTESIAN_POINT('',(0.,0.,-0.0166355706936178));
#41919=CARTESIAN_POINT('',(-0.008,0.,-0.0166355706936178));
#41920=CARTESIAN_POINT('',(0.,0.,-0.0166355706936178));
#41921=CARTESIAN_POINT('',(0.,0.,-0.0166355706936178));
#41922=CARTESIAN_POINT('',(0.,0.,-0.0166355706936178));
#41923=CARTESIAN_POINT('',(0.,0.,-0.0166355706936178));
#41924=CARTESIAN_POINT('',(-0.003,0.,-0.0110189377942895));
#41925=CARTESIAN_POINT('',(0.,0.,-0.0110189377942895));
#41926=CARTESIAN_POINT('',(0.,0.,-0.0110189377942895));
#41927=CARTESIAN_POINT('',(0.,0.,-0.0110189377942895));
#41928=CARTESIAN_POINT('',(0.,0.,-0.0110189377942895));
#41929=CARTESIAN_POINT('',(0.,0.,-0.0110189377942895));
#41930=CARTESIAN_POINT('',(-0.00180420299878392,0.,-0.0110189377942895));
#41931=CARTESIAN_POINT('',(0.,0.,-0.0150189377942895));
#41932=CARTESIAN_POINT('',(0.,0.,-0.0150189377942895));
#41933=CARTESIAN_POINT('',(0.,0.,-0.0150189377942895));
#41934=CARTESIAN_POINT('',(0.,0.,-0.0166355706936178));
#41935=CARTESIAN_POINT('',(0.,0.,-0.0166355706936178));
#41936=CARTESIAN_POINT('',(0.,0.,-0.0166355706936178));
#41937=CARTESIAN_POINT('',(0.,0.,-0.0300923697749146));
#41938=CARTESIAN_POINT('',(0.,0.,-0.0166355706936178));
#41939=CARTESIAN_POINT('',(0.,0.,-0.0300923697749146));
#41940=CARTESIAN_POINT('',(0.,0.,-0.0173355706936178));
#41941=CARTESIAN_POINT('',(-0.008,0.,-0.0173355706936178));
#41942=CARTESIAN_POINT('',(0.,0.,-0.0173355706936178));
#41943=CARTESIAN_POINT('',(0.,0.,-0.0150189377942895));
#45463=MECHANICAL_DESIGN_GEOMETRIC_PRESENTATION_REPRESENTATION('',(#13553),#45464);
#45464=(
GEOMETRIC_REPRESENTATION_CONTEXT(3)
GLOBAL_UNCERTAINTY_ASSIGNED_CONTEXT((#45492))
GLOBAL_UNIT_ASSIGNED_CONTEXT((#45522,#45521,#45520))
REPRESENTATION_CONTEXT('MAS-690','TOP_LEVEL_ASSEMBLY_PART')
);
#45489=(
GEOMETRIC_REPRESENTATION_CONTEXT(3)
GLOBAL_UNCERTAINTY_ASSIGNED_CONTEXT((#45517))
GLOBAL_UNIT_ASSIGNED_CONTEXT((#45522,#45521,#45520))
REPRESENTATION_CONTEXT('ball_retainer','COMPONENT_PART')
);
#45492=UNCERTAINTY_MEASURE_WITH_UNIT(LENGTH_MEASURE(1.E-8),#45522,
'DISTANCE_ACCURACY_VALUE','Maximum Tolerance applied to model');
#45517=UNCERTAINTY_MEASURE_WITH_UNIT(LENGTH_MEASURE(1.E-6),#45522,
'DISTANCE_ACCURACY_VALUE','Maximum Tolerance applied to model');
#45520=(
NAMED_UNIT(*)
SI_UNIT($,.STERADIAN.)
SOLID_ANGLE_UNIT()
);
#45521=(
NAMED_UNIT(*)
PLANE_ANGLE_UNIT()
SI_UNIT($,.RADIAN.)
);
#45522=(
LENGTH_UNIT()
NAMED_UNIT(*)
SI_UNIT($,.METRE.)
);
#45579=PRODUCT_DEFINITION_SHAPE('','',#45610);
#45610=PRODUCT_DEFINITION('','',#45666,#45638);
#45638=PRODUCT_DEFINITION_CONTEXT('',#45782,'design');
#45666=PRODUCT_DEFINITION_FORMATION_WITH_SPECIFIED_SOURCE('','',#45722,
 .NOT_KNOWN.);
#45722=PRODUCT('ball_retainer','ball_retainer','ball_retainer',(#45778));
#45778=PRODUCT_CONTEXT('',#45782,'mechanical');
#45782=APPLICATION_CONTEXT('managed model based 3d engineering');
ENDSEC;
END-ISO-10303-21;
